ISO-10303-21;
HEADER;
/* Generated by software containing ST-Developer
 * from STEP Tools, Inc. (www.steptools.com) 
 */

FILE_DESCRIPTION(
/* description */ ('Manual piston pump'),
/* implementation_level */ '2;1');

FILE_NAME(
/* name */ 'M4x10 Cap Screw.step',
/* time_stamp */ '2026-11-02T16:54:23-08:00',
/* author */ (''),
/* organization */ (''),
/* preprocessor_version */ 'ST-DEVELOPER v20.2',
/* originating_system */ 'Autodesk Translation Framework v15.17.0.0',
/* authorisation */ '');

FILE_SCHEMA (('AUTOMOTIVE_DESIGN { 1 0 10303 214 3 1 1 }'));
ENDSEC;

DATA;
#10=MECHANICAL_DESIGN_GEOMETRIC_PRESENTATION_REPRESENTATION('',(#758),#19043);
#526=ORIENTED_CLOSED_SHELL('',*,#9546,.F.);
#550=CONICAL_SURFACE('',#11435,0.325,0.785398163397448);
#551=CONICAL_SURFACE('',#11439,0.335,0.785398163397448);
#552=CONICAL_SURFACE('',#11443,0.21,0.463647609000806);
#557=BREP_WITH_VOIDS('Body1',#9547,(#526));
#623=SHAPE_REPRESENTATION_RELATIONSHIP('SRR','None',#19373,#686);
#686=ADVANCED_BREP_SHAPE_REPRESENTATION('',(#557),#19040);
#758=STYLED_ITEM('',(#19663),#557);
#1043=FACE_BOUND('',#2648,.T.);
#1286=CYLINDRICAL_SURFACE('',#11437,0.35);
#1287=CYLINDRICAL_SURFACE('',#11445,0.1954);
#1843=FACE_OUTER_BOUND('',#2634,.T.);
#1844=FACE_OUTER_BOUND('',#2635,.T.);
#1845=FACE_OUTER_BOUND('',#2636,.T.);
#1846=FACE_OUTER_BOUND('',#2637,.T.);
#1847=FACE_OUTER_BOUND('',#2638,.T.);
#1848=FACE_OUTER_BOUND('',#2639,.T.);
#1849=FACE_OUTER_BOUND('',#2640,.T.);
#1850=FACE_OUTER_BOUND('',#2641,.T.);
#1851=FACE_OUTER_BOUND('',#2642,.T.);
#1852=FACE_OUTER_BOUND('',#2643,.T.);
#1853=FACE_OUTER_BOUND('',#2644,.T.);
#1854=FACE_OUTER_BOUND('',#2645,.T.);
#1855=FACE_OUTER_BOUND('',#2646,.T.);
#1856=FACE_OUTER_BOUND('',#2647,.T.);
#1857=FACE_OUTER_BOUND('',#2649,.T.);
#1858=FACE_OUTER_BOUND('',#2650,.T.);
#2634=EDGE_LOOP('',(#8477,#8478,#8479,#8480));
#2635=EDGE_LOOP('',(#8481,#8482,#8483,#8484));
#2636=EDGE_LOOP('',(#8485,#8486,#8487,#8488));
#2637=EDGE_LOOP('',(#8489,#8490,#8491,#8492));
#2638=EDGE_LOOP('',(#8493,#8494,#8495,#8496));
#2639=EDGE_LOOP('',(#8497,#8498,#8499,#8500));
#2640=EDGE_LOOP('',(#8501,#8502,#8503,#8504,#8505,#8506));
#2641=EDGE_LOOP('',(#8507,#8508,#8509,#8510,#8511,#8512));
#2642=EDGE_LOOP('',(#8513));
#2643=EDGE_LOOP('',(#8514));
#2644=EDGE_LOOP('',(#8515,#8516,#8517,#8518));
#2645=EDGE_LOOP('',(#8519,#8520,#8521,#8522));
#2646=EDGE_LOOP('',(#8523,#8524,#8525,#8526));
#2647=EDGE_LOOP('',(#8527));
#2648=EDGE_LOOP('',(#8528));
#2649=EDGE_LOOP('',(#8529,#8530,#8531,#8532));
#2650=EDGE_LOOP('',(#8533,#8534,#8535,#8536));
#3132=CIRCLE('',#11432,0.1954);
#3133=CIRCLE('',#11434,0.3);
#3134=CIRCLE('',#11436,0.35);
#3135=CIRCLE('',#11438,0.35);
#3136=CIRCLE('',#11440,0.32);
#3137=CIRCLE('',#11442,0.22);
#3138=CIRCLE('',#11444,0.1954);
#3718=LINE('',#18769,#4322);
#3719=LINE('',#18771,#4323);
#3720=LINE('',#18773,#4324);
#3721=LINE('',#18774,#4325);
#3722=LINE('',#18777,#4326);
#3723=LINE('',#18779,#4327);
#3724=LINE('',#18780,#4328);
#3725=LINE('',#18783,#4329);
#3726=LINE('',#18785,#4330);
#3727=LINE('',#18786,#4331);
#3728=LINE('',#18789,#4332);
#3729=LINE('',#18791,#4333);
#3730=LINE('',#18792,#4334);
#3731=LINE('',#18795,#4335);
#3732=LINE('',#18797,#4336);
#3733=LINE('',#18798,#4337);
#3734=LINE('',#18800,#4338);
#3735=LINE('',#18801,#4339);
#3736=LINE('',#18813,#4340);
#3737=LINE('',#18817,#4341);
#3738=LINE('',#18821,#4342);
#3739=LINE('',#18828,#4343);
#3740=LINE('',#18830,#4344);
#4322=VECTOR('',#14428,1.);
#4323=VECTOR('',#14429,1.);
#4324=VECTOR('',#14430,1.);
#4325=VECTOR('',#14431,1.);
#4326=VECTOR('',#14434,1.);
#4327=VECTOR('',#14435,1.);
#4328=VECTOR('',#14436,1.);
#4329=VECTOR('',#14439,1.);
#4330=VECTOR('',#14440,1.);
#4331=VECTOR('',#14441,1.);
#4332=VECTOR('',#14444,1.);
#4333=VECTOR('',#14445,1.);
#4334=VECTOR('',#14446,1.);
#4335=VECTOR('',#14449,1.);
#4336=VECTOR('',#14450,1.);
#4337=VECTOR('',#14451,1.);
#4338=VECTOR('',#14454,1.);
#4339=VECTOR('',#14455,1.);
#4340=VECTOR('',#14472,0.325);
#4341=VECTOR('',#14477,0.35);
#4342=VECTOR('',#14482,0.335);
#4343=VECTOR('',#14491,0.21);
#4344=VECTOR('',#14494,0.2);
#5092=VERTEX_POINT('',#18767);
#5093=VERTEX_POINT('',#18768);
#5094=VERTEX_POINT('',#18770);
#5095=VERTEX_POINT('',#18772);
#5096=VERTEX_POINT('',#18776);
#5097=VERTEX_POINT('',#18778);
#5098=VERTEX_POINT('',#18782);
#5099=VERTEX_POINT('',#18784);
#5100=VERTEX_POINT('',#18788);
#5101=VERTEX_POINT('',#18790);
#5102=VERTEX_POINT('',#18794);
#5103=VERTEX_POINT('',#18796);
#5104=VERTEX_POINT('',#18805);
#5105=VERTEX_POINT('',#18808);
#5106=VERTEX_POINT('',#18811);
#5107=VERTEX_POINT('',#18815);
#5108=VERTEX_POINT('',#18819);
#5109=VERTEX_POINT('',#18823);
#5110=VERTEX_POINT('',#18826);
#6225=EDGE_CURVE('',#5092,#5093,#3718,.T.);
#6226=EDGE_CURVE('',#5093,#5094,#3719,.T.);
#6227=EDGE_CURVE('',#5094,#5095,#3720,.T.);
#6228=EDGE_CURVE('',#5092,#5095,#3721,.T.);
#6229=EDGE_CURVE('',#5093,#5096,#3722,.T.);
#6230=EDGE_CURVE('',#5096,#5097,#3723,.T.);
#6231=EDGE_CURVE('',#5097,#5094,#3724,.T.);
#6232=EDGE_CURVE('',#5096,#5098,#3725,.T.);
#6233=EDGE_CURVE('',#5098,#5099,#3726,.T.);
#6234=EDGE_CURVE('',#5099,#5097,#3727,.T.);
#6235=EDGE_CURVE('',#5098,#5100,#3728,.T.);
#6236=EDGE_CURVE('',#5100,#5101,#3729,.T.);
#6237=EDGE_CURVE('',#5101,#5099,#3730,.T.);
#6238=EDGE_CURVE('',#5100,#5102,#3731,.T.);
#6239=EDGE_CURVE('',#5102,#5103,#3732,.T.);
#6240=EDGE_CURVE('',#5103,#5101,#3733,.T.);
#6241=EDGE_CURVE('',#5102,#5092,#3734,.T.);
#6242=EDGE_CURVE('',#5095,#5103,#3735,.T.);
#6243=EDGE_CURVE('',#5104,#5104,#3132,.T.);
#6244=EDGE_CURVE('',#5105,#5105,#3133,.T.);
#6245=EDGE_CURVE('',#5106,#5106,#3134,.T.);
#6246=EDGE_CURVE('',#5106,#5105,#3736,.T.);
#6247=EDGE_CURVE('',#5107,#5107,#3135,.T.);
#6248=EDGE_CURVE('',#5107,#5106,#3737,.T.);
#6249=EDGE_CURVE('',#5108,#5108,#3136,.T.);
#6250=EDGE_CURVE('',#5108,#5107,#3738,.T.);
#6251=EDGE_CURVE('',#5109,#5109,#3137,.T.);
#6252=EDGE_CURVE('',#5110,#5110,#3138,.F.);
#6253=EDGE_CURVE('',#5110,#5109,#3739,.T.);
#6254=EDGE_CURVE('',#5104,#5110,#3740,.T.);
#8477=ORIENTED_EDGE('',*,*,#6225,.T.);
#8478=ORIENTED_EDGE('',*,*,#6226,.T.);
#8479=ORIENTED_EDGE('',*,*,#6227,.T.);
#8480=ORIENTED_EDGE('',*,*,#6228,.F.);
#8481=ORIENTED_EDGE('',*,*,#6229,.T.);
#8482=ORIENTED_EDGE('',*,*,#6230,.T.);
#8483=ORIENTED_EDGE('',*,*,#6231,.T.);
#8484=ORIENTED_EDGE('',*,*,#6226,.F.);
#8485=ORIENTED_EDGE('',*,*,#6232,.T.);
#8486=ORIENTED_EDGE('',*,*,#6233,.T.);
#8487=ORIENTED_EDGE('',*,*,#6234,.T.);
#8488=ORIENTED_EDGE('',*,*,#6230,.F.);
#8489=ORIENTED_EDGE('',*,*,#6235,.T.);
#8490=ORIENTED_EDGE('',*,*,#6236,.T.);
#8491=ORIENTED_EDGE('',*,*,#6237,.T.);
#8492=ORIENTED_EDGE('',*,*,#6233,.F.);
#8493=ORIENTED_EDGE('',*,*,#6238,.T.);
#8494=ORIENTED_EDGE('',*,*,#6239,.T.);
#8495=ORIENTED_EDGE('',*,*,#6240,.T.);
#8496=ORIENTED_EDGE('',*,*,#6236,.F.);
#8497=ORIENTED_EDGE('',*,*,#6241,.T.);
#8498=ORIENTED_EDGE('',*,*,#6228,.T.);
#8499=ORIENTED_EDGE('',*,*,#6242,.T.);
#8500=ORIENTED_EDGE('',*,*,#6239,.F.);
#8501=ORIENTED_EDGE('',*,*,#6241,.F.);
#8502=ORIENTED_EDGE('',*,*,#6238,.F.);
#8503=ORIENTED_EDGE('',*,*,#6235,.F.);
#8504=ORIENTED_EDGE('',*,*,#6232,.F.);
#8505=ORIENTED_EDGE('',*,*,#6229,.F.);
#8506=ORIENTED_EDGE('',*,*,#6225,.F.);
#8507=ORIENTED_EDGE('',*,*,#6242,.F.);
#8508=ORIENTED_EDGE('',*,*,#6227,.F.);
#8509=ORIENTED_EDGE('',*,*,#6231,.F.);
#8510=ORIENTED_EDGE('',*,*,#6234,.F.);
#8511=ORIENTED_EDGE('',*,*,#6237,.F.);
#8512=ORIENTED_EDGE('',*,*,#6240,.F.);
#8513=ORIENTED_EDGE('',*,*,#6243,.F.);
#8514=ORIENTED_EDGE('',*,*,#6244,.F.);
#8515=ORIENTED_EDGE('',*,*,#6245,.F.);
#8516=ORIENTED_EDGE('',*,*,#6246,.T.);
#8517=ORIENTED_EDGE('',*,*,#6244,.T.);
#8518=ORIENTED_EDGE('',*,*,#6246,.F.);
#8519=ORIENTED_EDGE('',*,*,#6247,.F.);
#8520=ORIENTED_EDGE('',*,*,#6248,.T.);
#8521=ORIENTED_EDGE('',*,*,#6245,.T.);
#8522=ORIENTED_EDGE('',*,*,#6248,.F.);
#8523=ORIENTED_EDGE('',*,*,#6249,.F.);
#8524=ORIENTED_EDGE('',*,*,#6250,.T.);
#8525=ORIENTED_EDGE('',*,*,#6247,.T.);
#8526=ORIENTED_EDGE('',*,*,#6250,.F.);
#8527=ORIENTED_EDGE('',*,*,#6249,.T.);
#8528=ORIENTED_EDGE('',*,*,#6251,.F.);
#8529=ORIENTED_EDGE('',*,*,#6252,.F.);
#8530=ORIENTED_EDGE('',*,*,#6253,.T.);
#8531=ORIENTED_EDGE('',*,*,#6251,.T.);
#8532=ORIENTED_EDGE('',*,*,#6253,.F.);
#8533=ORIENTED_EDGE('',*,*,#6243,.T.);
#8534=ORIENTED_EDGE('',*,*,#6254,.T.);
#8535=ORIENTED_EDGE('',*,*,#6252,.T.);
#8536=ORIENTED_EDGE('',*,*,#6254,.F.);
#8882=PLANE('',#11423);
#8883=PLANE('',#11424);
#8884=PLANE('',#11425);
#8885=PLANE('',#11426);
#8886=PLANE('',#11427);
#8887=PLANE('',#11428);
#8888=PLANE('',#11429);
#8889=PLANE('',#11430);
#8890=PLANE('',#11431);
#8891=PLANE('',#11433);
#8892=PLANE('',#11441);
#9448=ADVANCED_FACE('',(#1843),#8882,.F.);
#9449=ADVANCED_FACE('',(#1844),#8883,.F.);
#9450=ADVANCED_FACE('',(#1845),#8884,.F.);
#9451=ADVANCED_FACE('',(#1846),#8885,.F.);
#9452=ADVANCED_FACE('',(#1847),#8886,.F.);
#9453=ADVANCED_FACE('',(#1848),#8887,.F.);
#9454=ADVANCED_FACE('',(#1849),#8888,.F.);
#9455=ADVANCED_FACE('',(#1850),#8889,.F.);
#9456=ADVANCED_FACE('',(#1851),#8890,.F.);
#9457=ADVANCED_FACE('',(#1852),#8891,.T.);
#9458=ADVANCED_FACE('',(#1853),#550,.T.);
#9459=ADVANCED_FACE('',(#1854),#1286,.T.);
#9460=ADVANCED_FACE('',(#1855),#551,.T.);
#9461=ADVANCED_FACE('',(#1856,#1043),#8892,.T.);
#9462=ADVANCED_FACE('',(#1857),#552,.T.);
#9463=ADVANCED_FACE('',(#1858),#1287,.T.);
#9546=CLOSED_SHELL('',(#9448,#9449,#9450,#9451,#9452,#9453,#9454,#9455));
#9547=CLOSED_SHELL('',(#9456,#9457,#9458,#9459,#9460,#9461,#9462,#9463));
#11422=AXIS2_PLACEMENT_3D('',#18765,#14424,#14425);
#11423=AXIS2_PLACEMENT_3D('',#18766,#14426,#14427);
#11424=AXIS2_PLACEMENT_3D('',#18775,#14432,#14433);
#11425=AXIS2_PLACEMENT_3D('',#18781,#14437,#14438);
#11426=AXIS2_PLACEMENT_3D('',#18787,#14442,#14443);
#11427=AXIS2_PLACEMENT_3D('',#18793,#14447,#14448);
#11428=AXIS2_PLACEMENT_3D('',#18799,#14452,#14453);
#11429=AXIS2_PLACEMENT_3D('',#18802,#14456,#14457);
#11430=AXIS2_PLACEMENT_3D('',#18803,#14458,#14459);
#11431=AXIS2_PLACEMENT_3D('',#18804,#14460,#14461);
#11432=AXIS2_PLACEMENT_3D('',#18806,#14462,#14463);
#11433=AXIS2_PLACEMENT_3D('',#18807,#14464,#14465);
#11434=AXIS2_PLACEMENT_3D('',#18809,#14466,#14467);
#11435=AXIS2_PLACEMENT_3D('',#18810,#14468,#14469);
#11436=AXIS2_PLACEMENT_3D('',#18812,#14470,#14471);
#11437=AXIS2_PLACEMENT_3D('',#18814,#14473,#14474);
#11438=AXIS2_PLACEMENT_3D('',#18816,#14475,#14476);
#11439=AXIS2_PLACEMENT_3D('',#18818,#14478,#14479);
#11440=AXIS2_PLACEMENT_3D('',#18820,#14480,#14481);
#11441=AXIS2_PLACEMENT_3D('',#18822,#14483,#14484);
#11442=AXIS2_PLACEMENT_3D('',#18824,#14485,#14486);
#11443=AXIS2_PLACEMENT_3D('',#18825,#14487,#14488);
#11444=AXIS2_PLACEMENT_3D('',#18827,#14489,#14490);
#11445=AXIS2_PLACEMENT_3D('',#18829,#14492,#14493);
#14424=DIRECTION('axis',(0.,0.,1.));
#14425=DIRECTION('refdir',(1.,0.,0.));
#14426=DIRECTION('center_axis',(0.866025403784439,0.,-0.5));
#14427=DIRECTION('ref_axis',(0.5,0.,0.866025403784439));
#14428=DIRECTION('',(-0.5,0.,-0.866025403784439));
#14429=DIRECTION('',(0.,-1.,0.));
#14430=DIRECTION('',(0.5,0.,0.866025403784439));
#14431=DIRECTION('',(0.,-1.,0.));
#14432=DIRECTION('center_axis',(1.60246890531964E-16,0.,-1.));
#14433=DIRECTION('ref_axis',(1.,0.,1.60246890531964E-16));
#14434=DIRECTION('',(-1.,0.,-1.60246890531964E-16));
#14435=DIRECTION('',(0.,-1.,0.));
#14436=DIRECTION('',(1.,0.,1.60246890531964E-16));
#14437=DIRECTION('center_axis',(-0.866025403784439,0.,-0.5));
#14438=DIRECTION('ref_axis',(0.5,0.,-0.866025403784439));
#14439=DIRECTION('',(-0.5,0.,0.866025403784439));
#14440=DIRECTION('',(0.,-1.,0.));
#14441=DIRECTION('',(0.5,0.,-0.866025403784439));
#14442=DIRECTION('center_axis',(-0.866025403784439,0.,0.5));
#14443=DIRECTION('ref_axis',(-0.5,0.,-0.866025403784439));
#14444=DIRECTION('',(0.5,0.,0.866025403784439));
#14445=DIRECTION('',(0.,-1.,0.));
#14446=DIRECTION('',(-0.5,0.,-0.866025403784439));
#14447=DIRECTION('center_axis',(-1.60246890531964E-16,0.,1.));
#14448=DIRECTION('ref_axis',(-1.,0.,-1.60246890531964E-16));
#14449=DIRECTION('',(1.,0.,1.60246890531964E-16));
#14450=DIRECTION('',(0.,-1.,0.));
#14451=DIRECTION('',(-1.,0.,-1.60246890531964E-16));
#14452=DIRECTION('center_axis',(0.866025403784439,0.,0.5));
#14453=DIRECTION('ref_axis',(-0.5,0.,0.866025403784439));
#14454=DIRECTION('',(0.5,0.,-0.866025403784439));
#14455=DIRECTION('',(-0.5,0.,0.866025403784439));
#14456=DIRECTION('center_axis',(0.,1.,0.));
#14457=DIRECTION('ref_axis',(1.,0.,0.));
#14458=DIRECTION('center_axis',(0.,-1.,0.));
#14459=DIRECTION('ref_axis',(0.,0.,-1.));
#14460=DIRECTION('center_axis',(0.,1.,0.));
#14461=DIRECTION('ref_axis',(1.,0.,0.));
#14462=DIRECTION('center_axis',(0.,1.,0.));
#14463=DIRECTION('ref_axis',(1.,0.,0.));
#14464=DIRECTION('center_axis',(0.,1.,0.));
#14465=DIRECTION('ref_axis',(0.,0.,1.));
#14466=DIRECTION('center_axis',(0.,-1.,0.));
#14467=DIRECTION('ref_axis',(1.,0.,0.));
#14468=DIRECTION('center_axis',(0.,-1.,0.));
#14469=DIRECTION('ref_axis',(1.,0.,0.));
#14470=DIRECTION('center_axis',(0.,-1.,0.));
#14471=DIRECTION('ref_axis',(1.,0.,0.));
#14472=DIRECTION('',(0.707106781186547,0.707106781186548,8.65956056235493E-17));
#14473=DIRECTION('center_axis',(0.,-1.,0.));
#14474=DIRECTION('ref_axis',(1.,0.,0.));
#14475=DIRECTION('center_axis',(0.,-1.,0.));
#14476=DIRECTION('ref_axis',(1.,0.,0.));
#14477=DIRECTION('',(0.,1.,0.));
#14478=DIRECTION('center_axis',(0.,1.,0.));
#14479=DIRECTION('ref_axis',(1.,0.,0.));
#14480=DIRECTION('center_axis',(0.,-1.,0.));
#14481=DIRECTION('ref_axis',(1.,0.,0.));
#14482=DIRECTION('',(-0.707106781186547,0.707106781186548,-8.65956056235493E-17));
#14483=DIRECTION('center_axis',(0.,-1.,0.));
#14484=DIRECTION('ref_axis',(0.,0.,-1.));
#14485=DIRECTION('center_axis',(0.,-1.,0.));
#14486=DIRECTION('ref_axis',(1.,0.,0.));
#14487=DIRECTION('center_axis',(0.,1.,0.));
#14488=DIRECTION('ref_axis',(1.,0.,0.));
#14489=DIRECTION('center_axis',(0.,1.,0.));
#14490=DIRECTION('ref_axis',(1.,0.,0.));
#14491=DIRECTION('',(-0.447213595499958,0.894427190999916,-5.47678698264203E-17));
#14492=DIRECTION('center_axis',(0.,-1.,0.));
#14493=DIRECTION('ref_axis',(1.,0.,0.));
#14494=DIRECTION('',(0.,1.,0.));
#18765=CARTESIAN_POINT('',(0.,0.,0.));
#18766=CARTESIAN_POINT('Origin',(0.0866025403784439,-0.4,-0.15));
#18767=CARTESIAN_POINT('',(0.173205080756888,-0.4,0.));
#18768=CARTESIAN_POINT('',(0.0866025403784439,-0.4,-0.15));
#18769=CARTESIAN_POINT('',(0.173205080756888,-0.4,0.));
#18770=CARTESIAN_POINT('',(0.0866025403784439,-0.64,-0.15));
#18771=CARTESIAN_POINT('',(0.0866025403784439,-0.4,-0.15));
#18772=CARTESIAN_POINT('',(0.173205080756888,-0.64,0.));
#18773=CARTESIAN_POINT('',(0.173205080756888,-0.64,0.));
#18774=CARTESIAN_POINT('',(0.173205080756888,-0.4,0.));
#18775=CARTESIAN_POINT('Origin',(-0.0866025403784438,-0.4,-0.15));
#18776=CARTESIAN_POINT('',(-0.0866025403784438,-0.4,-0.15));
#18777=CARTESIAN_POINT('',(0.0866025403784439,-0.4,-0.15));
#18778=CARTESIAN_POINT('',(-0.0866025403784438,-0.64,-0.15));
#18779=CARTESIAN_POINT('',(-0.0866025403784438,-0.4,-0.15));
#18780=CARTESIAN_POINT('',(0.0866025403784439,-0.64,-0.15));
#18781=CARTESIAN_POINT('Origin',(-0.173205080756888,-0.4,-2.77555756156289E-17));
#18782=CARTESIAN_POINT('',(-0.173205080756888,-0.4,-2.12115047744981E-17));
#18783=CARTESIAN_POINT('',(-0.0866025403784438,-0.4,-0.15));
#18784=CARTESIAN_POINT('',(-0.173205080756888,-0.64,-2.77555756156289E-17));
#18785=CARTESIAN_POINT('',(-0.173205080756888,-0.4,-2.12115047744981E-17));
#18786=CARTESIAN_POINT('',(-0.0866025403784438,-0.64,-0.15));
#18787=CARTESIAN_POINT('Origin',(-0.0866025403784439,-0.4,0.15));
#18788=CARTESIAN_POINT('',(-0.0866025403784439,-0.4,0.15));
#18789=CARTESIAN_POINT('',(-0.173205080756888,-0.4,-2.12115047744981E-17));
#18790=CARTESIAN_POINT('',(-0.0866025403784439,-0.64,0.15));
#18791=CARTESIAN_POINT('',(-0.0866025403784439,-0.4,0.15));
#18792=CARTESIAN_POINT('',(-0.173205080756888,-0.64,-2.12115047744981E-17));
#18793=CARTESIAN_POINT('Origin',(0.0866025403784439,-0.4,0.15));
#18794=CARTESIAN_POINT('',(0.0866025403784439,-0.4,0.15));
#18795=CARTESIAN_POINT('',(-0.0866025403784439,-0.4,0.15));
#18796=CARTESIAN_POINT('',(0.0866025403784439,-0.64,0.15));
#18797=CARTESIAN_POINT('',(0.0866025403784439,-0.4,0.15));
#18798=CARTESIAN_POINT('',(-0.0866025403784439,-0.64,0.15));
#18799=CARTESIAN_POINT('Origin',(0.173205080756888,-0.4,0.));
#18800=CARTESIAN_POINT('',(0.0866025403784439,-0.4,0.15));
#18801=CARTESIAN_POINT('',(0.0866025403784439,-0.64,0.15));
#18802=CARTESIAN_POINT('Origin',(0.,-0.4,-2.77555756156289E-17));
#18803=CARTESIAN_POINT('Origin',(0.,-0.64,-2.77555756156289E-17));
#18804=CARTESIAN_POINT('Origin',(0.,-1.,0.));
#18805=CARTESIAN_POINT('',(-0.1954,-1.,2.39295984553393E-17));
#18806=CARTESIAN_POINT('Origin',(0.,-1.,0.));
#18807=CARTESIAN_POINT('Origin',(0.3,0.4,0.));
#18808=CARTESIAN_POINT('',(-0.3,0.4,-3.67394039744206E-17));
#18809=CARTESIAN_POINT('Origin',(0.,0.4,0.));
#18810=CARTESIAN_POINT('Origin',(0.,0.375,0.));
#18811=CARTESIAN_POINT('',(-0.35,0.35,-4.28626379701573E-17));
#18812=CARTESIAN_POINT('Origin',(0.,0.35,0.));
#18813=CARTESIAN_POINT('',(-0.325,0.375,-3.9801020972289E-17));
#18814=CARTESIAN_POINT('Origin',(0.,0.19,0.));
#18815=CARTESIAN_POINT('',(-0.35,0.03,-4.28626379701574E-17));
#18816=CARTESIAN_POINT('Origin',(0.,0.03,0.));
#18817=CARTESIAN_POINT('',(-0.35,0.19,-4.28626379701574E-17));
#18818=CARTESIAN_POINT('Origin',(0.,0.0149999999999999,0.));
#18819=CARTESIAN_POINT('',(-0.32,-3.29597460435593E-17,-3.91886975727153E-17));
#18820=CARTESIAN_POINT('Origin',(0.,0.,0.));
#18821=CARTESIAN_POINT('',(-0.335,0.0149999999999999,-4.10256677714363E-17));
#18822=CARTESIAN_POINT('Origin',(0.22,0.,0.));
#18823=CARTESIAN_POINT('',(-0.22,-6.93889390390723E-18,-2.69422295812418E-17));
#18824=CARTESIAN_POINT('Origin',(0.,0.,0.));
#18825=CARTESIAN_POINT('Origin',(0.,-0.02,0.));
#18826=CARTESIAN_POINT('',(-0.1954,-0.0492,2.39295984553393E-17));
#18827=CARTESIAN_POINT('Origin',(0.,-0.0492,0.));
#18828=CARTESIAN_POINT('',(-0.21,-0.02,-2.57175827820944E-17));
#18829=CARTESIAN_POINT('Origin',(0.,-0.8,0.));
#18830=CARTESIAN_POINT('',(-0.1954,-0.8,-2.39295984553393E-17));
#18969=UNCERTAINTY_MEASURE_WITH_UNIT(LENGTH_MEASURE(0.001),#19044,
'DISTANCE_ACCURACY_VALUE',
'Maximum model space distance between geometric entities at asserted c
onnectivities');
#18972=UNCERTAINTY_MEASURE_WITH_UNIT(LENGTH_MEASURE(0.001),#19044,
'DISTANCE_ACCURACY_VALUE',
'Maximum model space distance between geometric entities at asserted c
onnectivities');
#19040=(
GEOMETRIC_REPRESENTATION_CONTEXT(3)
GLOBAL_UNCERTAINTY_ASSIGNED_CONTEXT((#18969))
GLOBAL_UNIT_ASSIGNED_CONTEXT((#19044,#19046,#19047))
REPRESENTATION_CONTEXT('','3D')
);
#19043=(
GEOMETRIC_REPRESENTATION_CONTEXT(3)
GLOBAL_UNCERTAINTY_ASSIGNED_CONTEXT((#18972))
GLOBAL_UNIT_ASSIGNED_CONTEXT((#19044,#19046,#19047))
REPRESENTATION_CONTEXT('','3D')
);
#19044=(
LENGTH_UNIT()
NAMED_UNIT(*)
SI_UNIT(.CENTI.,.METRE.)
);
#19046=(
NAMED_UNIT(*)
PLANE_ANGLE_UNIT()
SI_UNIT($,.RADIAN.)
);
#19047=(
NAMED_UNIT(*)
SI_UNIT($,.STERADIAN.)
SOLID_ANGLE_UNIT()
);
#19115=SHAPE_DEFINITION_REPRESENTATION(#19272,#19373);
#19272=PRODUCT_DEFINITION_SHAPE('',$,#19444);
#19373=SHAPE_REPRESENTATION('',(#11422),#19040);
#19376=PRODUCT_DEFINITION_CONTEXT('part definition',#19588,'design');
#19444=PRODUCT_DEFINITION('2026-11-03-00-38-46-518','M4x10 Cap Screw',#19514,
#19376);
#19514=PRODUCT_DEFINITION_FORMATION('',$,#19657);
#19588=APPLICATION_CONTEXT(
'Core Data for Automotive Mechanical Design Process');
#19589=PRODUCT_CONTEXT('part definition',#19588,'mechanical');
#19657=PRODUCT('2026-11-03-00-38-46-518','M4x10 Cap Screw',
'M4x10 Cap Screw',(#19589));
#19663=PRESENTATION_STYLE_ASSIGNMENT((#19669));
#19669=SURFACE_STYLE_USAGE(.BOTH.,#19675);
#19675=SURFACE_SIDE_STYLE('',(#19681));
#19681=SURFACE_STYLE_FILL_AREA(#19687);
#19687=FILL_AREA_STYLE('CAD Library Painted - Graphite',(#19693));
#19693=FILL_AREA_STYLE_COLOUR('CAD Library Painted - Graphite',#19699);
#19699=COLOUR_RGB('CAD Library Painted - Graphite',0.168627450980392,0.192156862745098,
0.231372549019608);
ENDSEC;
END-ISO-10303-21;
